ISO-10303-21;
HEADER;
/* Generated by software containing ST-Developer
 * from STEP Tools, Inc. (www.steptools.com) 
 */

FILE_DESCRIPTION(
/* description */ ('Double-row support with tensioned shaft'),
/* implementation_level */ '2;1');

FILE_NAME(
/* name */ 'Flange hole reducer (3).step',
/* time_stamp */ '2026-10-27T10:50:35-07:00',
/* author */ (''),
/* organization */ (''),
/* preprocessor_version */ 'ST-DEVELOPER v20.2',
/* originating_system */ 'Autodesk Translation Framework v15.17.0.0',
/* authorisation */ '');

FILE_SCHEMA (('AUTOMOTIVE_DESIGN { 1 0 10303 214 3 1 1 }'));
ENDSEC;

DATA;
#10=MECHANICAL_DESIGN_GEOMETRIC_PRESENTATION_REPRESENTATION('',(#488),#11559);
#424=SHAPE_REPRESENTATION_RELATIONSHIP('SRR','None',#11732,#456);
#456=ADVANCED_BREP_SHAPE_REPRESENTATION('',(#521),#11534);
#488=STYLED_ITEM('',(#11981),#521);
#521=MANIFOLD_SOLID_BREP('Body1',#6333);
#586=FACE_BOUND('',#1377,.T.);
#587=FACE_BOUND('',#1379,.T.);
#723=PLANE('',#6850);
#724=PLANE('',#6851);
#986=FACE_OUTER_BOUND('',#1374,.T.);
#987=FACE_OUTER_BOUND('',#1375,.T.);
#988=FACE_OUTER_BOUND('',#1376,.T.);
#989=FACE_OUTER_BOUND('',#1378,.T.);
#1374=EDGE_LOOP('',(#4636,#4637,#4638,#4639));
#1375=EDGE_LOOP('',(#4640,#4641,#4642,#4643));
#1376=EDGE_LOOP('',(#4644));
#1377=EDGE_LOOP('',(#4645));
#1378=EDGE_LOOP('',(#4646));
#1379=EDGE_LOOP('',(#4647));
#1845=LINE('',#9574,#2392);
#1846=LINE('',#9580,#2393);
#2392=VECTOR('',#7740,0.425);
#2393=VECTOR('',#7747,0.595);
#2886=CIRCLE('',#6845,0.425);
#2887=CIRCLE('',#6846,0.425);
#2888=CIRCLE('',#6848,0.595);
#2889=CIRCLE('',#6849,0.595);
#3129=VERTEX_POINT('',#9571);
#3130=VERTEX_POINT('',#9573);
#3131=VERTEX_POINT('',#9577);
#3132=VERTEX_POINT('',#9579);
#3703=EDGE_CURVE('',#3129,#3129,#2886,.T.);
#3704=EDGE_CURVE('',#3129,#3130,#1845,.T.);
#3705=EDGE_CURVE('',#3130,#3130,#2887,.T.);
#3706=EDGE_CURVE('',#3131,#3131,#2888,.T.);
#3707=EDGE_CURVE('',#3131,#3132,#1846,.T.);
#3708=EDGE_CURVE('',#3132,#3132,#2889,.T.);
#4636=ORIENTED_EDGE('',*,*,#3703,.F.);
#4637=ORIENTED_EDGE('',*,*,#3704,.T.);
#4638=ORIENTED_EDGE('',*,*,#3705,.T.);
#4639=ORIENTED_EDGE('',*,*,#3704,.F.);
#4640=ORIENTED_EDGE('',*,*,#3706,.F.);
#4641=ORIENTED_EDGE('',*,*,#3707,.T.);
#4642=ORIENTED_EDGE('',*,*,#3708,.T.);
#4643=ORIENTED_EDGE('',*,*,#3707,.F.);
#4644=ORIENTED_EDGE('',*,*,#3706,.T.);
#4645=ORIENTED_EDGE('',*,*,#3703,.T.);
#4646=ORIENTED_EDGE('',*,*,#3708,.F.);
#4647=ORIENTED_EDGE('',*,*,#3705,.F.);
#5915=CYLINDRICAL_SURFACE('',#6844,0.425);
#5916=CYLINDRICAL_SURFACE('',#6847,0.595);
#6049=ADVANCED_FACE('',(#986),#5915,.F.);
#6050=ADVANCED_FACE('',(#987),#5916,.T.);
#6051=ADVANCED_FACE('',(#988,#586),#723,.T.);
#6052=ADVANCED_FACE('',(#989,#587),#724,.F.);
#6333=CLOSED_SHELL('',(#6049,#6050,#6051,#6052));
#6843=AXIS2_PLACEMENT_3D('',#9569,#7734,#7735);
#6844=AXIS2_PLACEMENT_3D('',#9570,#7736,#7737);
#6845=AXIS2_PLACEMENT_3D('',#9572,#7738,#7739);
#6846=AXIS2_PLACEMENT_3D('',#9575,#7741,#7742);
#6847=AXIS2_PLACEMENT_3D('',#9576,#7743,#7744);
#6848=AXIS2_PLACEMENT_3D('',#9578,#7745,#7746);
#6849=AXIS2_PLACEMENT_3D('',#9581,#7748,#7749);
#6850=AXIS2_PLACEMENT_3D('',#9582,#7750,#7751);
#6851=AXIS2_PLACEMENT_3D('',#9583,#7752,#7753);
#7734=DIRECTION('axis',(0.,0.,1.));
#7735=DIRECTION('refdir',(1.,0.,0.));
#7736=DIRECTION('center_axis',(0.,1.,0.));
#7737=DIRECTION('ref_axis',(1.,0.,0.));
#7738=DIRECTION('center_axis',(0.,-1.,0.));
#7739=DIRECTION('ref_axis',(1.,0.,0.));
#7740=DIRECTION('',(0.,-1.,0.));
#7741=DIRECTION('center_axis',(0.,-1.,0.));
#7742=DIRECTION('ref_axis',(1.,0.,0.));
#7743=DIRECTION('center_axis',(0.,1.,0.));
#7744=DIRECTION('ref_axis',(1.,0.,0.));
#7745=DIRECTION('center_axis',(0.,1.,0.));
#7746=DIRECTION('ref_axis',(1.,0.,0.));
#7747=DIRECTION('',(0.,-1.,0.));
#7748=DIRECTION('center_axis',(0.,1.,0.));
#7749=DIRECTION('ref_axis',(1.,0.,0.));
#7750=DIRECTION('center_axis',(0.,1.,0.));
#7751=DIRECTION('ref_axis',(1.,0.,0.));
#7752=DIRECTION('center_axis',(0.,1.,0.));
#7753=DIRECTION('ref_axis',(1.,0.,0.));
#9569=CARTESIAN_POINT('',(0.,0.,0.));
#9570=CARTESIAN_POINT('Origin',(3.2,-0.5,13.2));
#9571=CARTESIAN_POINT('',(2.775,0.5,13.2));
#9572=CARTESIAN_POINT('Origin',(3.2,0.5,13.2));
#9573=CARTESIAN_POINT('',(2.775,-0.5,13.2));
#9574=CARTESIAN_POINT('',(2.775,-0.5,13.2));
#9575=CARTESIAN_POINT('Origin',(3.2,-0.5,13.2));
#9576=CARTESIAN_POINT('Origin',(3.2,-0.5,13.2));
#9577=CARTESIAN_POINT('',(2.605,0.5,13.2));
#9578=CARTESIAN_POINT('Origin',(3.2,0.5,13.2));
#9579=CARTESIAN_POINT('',(2.605,-0.5,13.2));
#9580=CARTESIAN_POINT('',(2.605,-0.5,13.2));
#9581=CARTESIAN_POINT('Origin',(3.2,-0.5,13.2));
#9582=CARTESIAN_POINT('Origin',(3.2,0.5,13.2));
#9583=CARTESIAN_POINT('Origin',(3.2,-0.5,13.2));
#11497=UNCERTAINTY_MEASURE_WITH_UNIT(LENGTH_MEASURE(0.001),#11560,
'DISTANCE_ACCURACY_VALUE',
'Maximum model space distance between geometric entities at asserted c
onnectivities');
#11522=UNCERTAINTY_MEASURE_WITH_UNIT(LENGTH_MEASURE(0.001),#11560,
'DISTANCE_ACCURACY_VALUE',
'Maximum model space distance between geometric entities at asserted c
onnectivities');
#11534=(
GEOMETRIC_REPRESENTATION_CONTEXT(3)
GLOBAL_UNCERTAINTY_ASSIGNED_CONTEXT((#11497))
GLOBAL_UNIT_ASSIGNED_CONTEXT((#11560,#11562,#11563))
REPRESENTATION_CONTEXT('','3D')
);
#11559=(
GEOMETRIC_REPRESENTATION_CONTEXT(3)
GLOBAL_UNCERTAINTY_ASSIGNED_CONTEXT((#11522))
GLOBAL_UNIT_ASSIGNED_CONTEXT((#11560,#11562,#11563))
REPRESENTATION_CONTEXT('','3D')
);
#11560=(
LENGTH_UNIT()
NAMED_UNIT(*)
SI_UNIT(.CENTI.,.METRE.)
);
#11562=(
NAMED_UNIT(*)
PLANE_ANGLE_UNIT()
SI_UNIT($,.RADIAN.)
);
#11563=(
NAMED_UNIT(*)
SI_UNIT($,.STERADIAN.)
SOLID_ANGLE_UNIT()
);
#11575=SHAPE_DEFINITION_REPRESENTATION(#11611,#11732);
#11611=PRODUCT_DEFINITION_SHAPE('',$,#11769);
#11732=SHAPE_REPRESENTATION('',(#6843),#11534);
#11757=PRODUCT_DEFINITION_CONTEXT('part definition',#11867,'design');
#11769=PRODUCT_DEFINITION('Flange hole reducer (3)',
'Flange hole reducer (3)',#11805,#11757);
#11805=PRODUCT_DEFINITION_FORMATION('',$,#11880);
#11867=APPLICATION_CONTEXT(
'Core Data for Automotive Mechanical Design Process');
#11868=PRODUCT_CONTEXT('part definition',#11867,'mechanical');
#11880=PRODUCT('Flange hole reducer (3)','Flange hole reducer (3)',
'Flange hole reducer (3)',(#11868));
#11975=COLOUR_RGB('Off White',0.89,0.88,0.83);
#11976=FILL_AREA_STYLE_COLOUR('',#11975);
#11977=FILL_AREA_STYLE('',(#11976));
#11978=SURFACE_STYLE_FILL_AREA(#11977);
#11979=SURFACE_SIDE_STYLE('',(#11978));
#11980=SURFACE_STYLE_USAGE(.BOTH.,#11979);
#11981=PRESENTATION_STYLE_ASSIGNMENT((#11980));
ENDSEC;
END-ISO-10303-21;
